ISO-10303-21;
HEADER;
/* Generated by software containing ST-Developer
 * from STEP Tools, Inc. (www.steptools.com) 
 */

FILE_DESCRIPTION(
/* description */ ('Four-bar parallelogram arm'),
/* implementation_level */ '2;1');

FILE_NAME(
/* name */ 'Inner race sleeve (2).step',
/* time_stamp */ '2026-10-28T03:24:55-07:00',
/* author */ (''),
/* organization */ (''),
/* preprocessor_version */ 'ST-DEVELOPER v20.2',
/* originating_system */ 'Autodesk Translation Framework v15.17.0.0',
/* authorisation */ '');

FILE_SCHEMA (('AUTOMOTIVE_DESIGN { 1 0 10303 214 3 1 1 }'));
ENDSEC;

DATA;
#10=MECHANICAL_DESIGN_GEOMETRIC_PRESENTATION_REPRESENTATION('',(#670),#14512);
#562=SHAPE_REPRESENTATION_RELATIONSHIP('SRR','None',#14787,#612);
#612=ADVANCED_BREP_SHAPE_REPRESENTATION('',(#726),#14502);
#670=STYLED_ITEM('',(#15087),#726);
#726=MANIFOLD_SOLID_BREP('Body1',#7376);
#980=FACE_BOUND('',#2228,.T.);
#981=FACE_BOUND('',#2230,.T.);
#1169=PLANE('',#8800);
#1170=PLANE('',#8801);
#1560=FACE_OUTER_BOUND('',#2225,.T.);
#1561=FACE_OUTER_BOUND('',#2226,.T.);
#1562=FACE_OUTER_BOUND('',#2227,.T.);
#1563=FACE_OUTER_BOUND('',#2229,.T.);
#2225=EDGE_LOOP('',(#6512,#6513,#6514,#6515));
#2226=EDGE_LOOP('',(#6516,#6517,#6518,#6519));
#2227=EDGE_LOOP('',(#6520));
#2228=EDGE_LOOP('',(#6521));
#2229=EDGE_LOOP('',(#6522));
#2230=EDGE_LOOP('',(#6523));
#2659=LINE('',#14114,#3053);
#2660=LINE('',#14120,#3054);
#3053=VECTOR('',#11033,0.504999999999999);
#3054=VECTOR('',#11040,0.699999999999999);
#3491=CIRCLE('',#8795,0.504999999999999);
#3492=CIRCLE('',#8796,0.504999999999999);
#3493=CIRCLE('',#8798,0.699999999999999);
#3494=CIRCLE('',#8799,0.699999999999999);
#4059=VERTEX_POINT('',#14111);
#4060=VERTEX_POINT('',#14113);
#4061=VERTEX_POINT('',#14117);
#4062=VERTEX_POINT('',#14119);
#4887=EDGE_CURVE('',#4059,#4059,#3491,.T.);
#4888=EDGE_CURVE('',#4059,#4060,#2659,.T.);
#4889=EDGE_CURVE('',#4060,#4060,#3492,.T.);
#4890=EDGE_CURVE('',#4061,#4061,#3493,.T.);
#4891=EDGE_CURVE('',#4061,#4062,#2660,.T.);
#4892=EDGE_CURVE('',#4062,#4062,#3494,.T.);
#6512=ORIENTED_EDGE('',*,*,#4887,.F.);
#6513=ORIENTED_EDGE('',*,*,#4888,.T.);
#6514=ORIENTED_EDGE('',*,*,#4889,.T.);
#6515=ORIENTED_EDGE('',*,*,#4888,.F.);
#6516=ORIENTED_EDGE('',*,*,#4890,.F.);
#6517=ORIENTED_EDGE('',*,*,#4891,.T.);
#6518=ORIENTED_EDGE('',*,*,#4892,.T.);
#6519=ORIENTED_EDGE('',*,*,#4891,.F.);
#6520=ORIENTED_EDGE('',*,*,#4890,.T.);
#6521=ORIENTED_EDGE('',*,*,#4887,.T.);
#6522=ORIENTED_EDGE('',*,*,#4892,.F.);
#6523=ORIENTED_EDGE('',*,*,#4889,.F.);
#6881=CYLINDRICAL_SURFACE('',#8794,0.504999999999999);
#6882=CYLINDRICAL_SURFACE('',#8797,0.699999999999999);
#7265=ADVANCED_FACE('',(#1560),#6881,.F.);
#7266=ADVANCED_FACE('',(#1561),#6882,.T.);
#7267=ADVANCED_FACE('',(#1562,#980),#1169,.T.);
#7268=ADVANCED_FACE('',(#1563,#981),#1170,.F.);
#7376=CLOSED_SHELL('',(#7265,#7266,#7267,#7268));
#8793=AXIS2_PLACEMENT_3D('',#14109,#11027,#11028);
#8794=AXIS2_PLACEMENT_3D('',#14110,#11029,#11030);
#8795=AXIS2_PLACEMENT_3D('',#14112,#11031,#11032);
#8796=AXIS2_PLACEMENT_3D('',#14115,#11034,#11035);
#8797=AXIS2_PLACEMENT_3D('',#14116,#11036,#11037);
#8798=AXIS2_PLACEMENT_3D('',#14118,#11038,#11039);
#8799=AXIS2_PLACEMENT_3D('',#14121,#11041,#11042);
#8800=AXIS2_PLACEMENT_3D('',#14122,#11043,#11044);
#8801=AXIS2_PLACEMENT_3D('',#14123,#11045,#11046);
#11027=DIRECTION('axis',(0.,0.,1.));
#11028=DIRECTION('refdir',(1.,0.,0.));
#11029=DIRECTION('center_axis',(0.,1.,0.));
#11030=DIRECTION('ref_axis',(1.,0.,0.));
#11031=DIRECTION('center_axis',(0.,-1.,0.));
#11032=DIRECTION('ref_axis',(1.,0.,0.));
#11033=DIRECTION('',(0.,-1.,0.));
#11034=DIRECTION('center_axis',(0.,-1.,0.));
#11035=DIRECTION('ref_axis',(1.,0.,0.));
#11036=DIRECTION('center_axis',(0.,1.,0.));
#11037=DIRECTION('ref_axis',(1.,0.,0.));
#11038=DIRECTION('center_axis',(0.,1.,0.));
#11039=DIRECTION('ref_axis',(1.,0.,0.));
#11040=DIRECTION('',(0.,-1.,0.));
#11041=DIRECTION('center_axis',(0.,1.,0.));
#11042=DIRECTION('ref_axis',(1.,0.,0.));
#11043=DIRECTION('center_axis',(0.,1.,0.));
#11044=DIRECTION('ref_axis',(1.,0.,0.));
#11045=DIRECTION('center_axis',(0.,1.,0.));
#11046=DIRECTION('ref_axis',(1.,0.,0.));
#14109=CARTESIAN_POINT('',(0.,0.,0.));
#14110=CARTESIAN_POINT('Origin',(20.,-0.15,8.));
#14111=CARTESIAN_POINT('',(19.495,0.15,8.));
#14112=CARTESIAN_POINT('Origin',(20.,0.15,8.));
#14113=CARTESIAN_POINT('',(19.495,-0.15,8.));
#14114=CARTESIAN_POINT('',(19.495,-0.15,8.));
#14115=CARTESIAN_POINT('Origin',(20.,-0.15,8.));
#14116=CARTESIAN_POINT('Origin',(20.,-0.15,8.));
#14117=CARTESIAN_POINT('',(19.3,0.15,8.));
#14118=CARTESIAN_POINT('Origin',(20.,0.15,8.));
#14119=CARTESIAN_POINT('',(19.3,-0.15,8.));
#14120=CARTESIAN_POINT('',(19.3,-0.15,8.));
#14121=CARTESIAN_POINT('Origin',(20.,-0.15,8.));
#14122=CARTESIAN_POINT('Origin',(20.,0.15,8.));
#14123=CARTESIAN_POINT('Origin',(20.,-0.15,8.));
#14445=UNCERTAINTY_MEASURE_WITH_UNIT(LENGTH_MEASURE(0.001),#14513,
'DISTANCE_ACCURACY_VALUE',
'Maximum model space distance between geometric entities at asserted c
onnectivities');
#14455=UNCERTAINTY_MEASURE_WITH_UNIT(LENGTH_MEASURE(0.001),#14513,
'DISTANCE_ACCURACY_VALUE',
'Maximum model space distance between geometric entities at asserted c
onnectivities');
#14502=(
GEOMETRIC_REPRESENTATION_CONTEXT(3)
GLOBAL_UNCERTAINTY_ASSIGNED_CONTEXT((#14445))
GLOBAL_UNIT_ASSIGNED_CONTEXT((#14513,#14515,#14516))
REPRESENTATION_CONTEXT('','3D')
);
#14512=(
GEOMETRIC_REPRESENTATION_CONTEXT(3)
GLOBAL_UNCERTAINTY_ASSIGNED_CONTEXT((#14455))
GLOBAL_UNIT_ASSIGNED_CONTEXT((#14513,#14515,#14516))
REPRESENTATION_CONTEXT('','3D')
);
#14513=(
LENGTH_UNIT()
NAMED_UNIT(*)
SI_UNIT(.CENTI.,.METRE.)
);
#14515=(
NAMED_UNIT(*)
PLANE_ANGLE_UNIT()
SI_UNIT($,.RADIAN.)
);
#14516=(
NAMED_UNIT(*)
SI_UNIT($,.STERADIAN.)
SOLID_ANGLE_UNIT()
);
#14563=SHAPE_DEFINITION_REPRESENTATION(#14679,#14787);
#14679=PRODUCT_DEFINITION_SHAPE('',$,#14844);
#14787=SHAPE_REPRESENTATION('',(#8793),#14502);
#14797=PRODUCT_DEFINITION_CONTEXT('part definition',#14967,'design');
#14844=PRODUCT_DEFINITION('Inner race sleeve (2)','Inner race sleeve (2)',
#14900,#14797);
#14900=PRODUCT_DEFINITION_FORMATION('',$,#15015);
#14967=APPLICATION_CONTEXT(
'Core Data for Automotive Mechanical Design Process');
#14968=PRODUCT_CONTEXT('part definition',#14967,'mechanical');
#15015=PRODUCT('Inner race sleeve (2)','Inner race sleeve (2)',
'Inner race sleeve (2)',(#14968));
#15081=COLOUR_RGB('Grey',0.48,0.52,0.57);
#15082=FILL_AREA_STYLE_COLOUR('',#15081);
#15083=FILL_AREA_STYLE('',(#15082));
#15084=SURFACE_STYLE_FILL_AREA(#15083);
#15085=SURFACE_SIDE_STYLE('',(#15084));
#15086=SURFACE_STYLE_USAGE(.BOTH.,#15085);
#15087=PRESENTATION_STYLE_ASSIGNMENT((#15086));
ENDSEC;
END-ISO-10303-21;
